ISO-10303-21;
HEADER;
/* Generated by software containing ST-Developer
 * from STEP Tools, Inc. (www.steptools.com) 
 */

FILE_DESCRIPTION(
/* description */ ('Worm-less right-angle friction wheel drive'),
/* implementation_level */ '2;1');

FILE_NAME(
/* name */ 'Output bearing carrier (1).step',
/* time_stamp */ '2026-10-28T03:22:36-07:00',
/* author */ (''),
/* organization */ (''),
/* preprocessor_version */ 'ST-DEVELOPER v20.2',
/* originating_system */ 'Autodesk Translation Framework v15.17.0.0',
/* authorisation */ '');

FILE_SCHEMA (('AUTOMOTIVE_DESIGN { 1 0 10303 214 3 1 1 }'));
ENDSEC;

DATA;
#10=MECHANICAL_DESIGN_GEOMETRIC_PRESENTATION_REPRESENTATION('',(#624),#17046);
#530=SHAPE_REPRESENTATION_RELATIONSHIP('SRR','None',#17273,#577);
#577=ADVANCED_BREP_SHAPE_REPRESENTATION('',(#678),#17009);
#624=STYLED_ITEM('',(#17591),#678);
#678=MANIFOLD_SOLID_BREP('Body1',#8179);
#859=FACE_BOUND('',#1991,.T.);
#860=FACE_BOUND('',#1993,.T.);
#861=FACE_BOUND('',#1998,.T.);
#862=FACE_BOUND('',#1999,.T.);
#863=FACE_BOUND('',#2000,.T.);
#864=FACE_BOUND('',#2001,.T.);
#865=FACE_BOUND('',#2002,.T.);
#866=FACE_BOUND('',#2005,.T.);
#867=FACE_BOUND('',#2006,.T.);
#868=FACE_BOUND('',#2007,.T.);
#869=FACE_BOUND('',#2008,.T.);
#870=FACE_BOUND('',#2009,.T.);
#871=FACE_BOUND('',#2012,.T.);
#872=FACE_BOUND('',#2013,.T.);
#1032=PLANE('',#9114);
#1033=PLANE('',#9115);
#1034=PLANE('',#9116);
#1035=PLANE('',#9117);
#1036=PLANE('',#9118);
#1037=PLANE('',#9119);
#1038=PLANE('',#9120);
#1039=PLANE('',#9121);
#1040=PLANE('',#9122);
#1041=PLANE('',#9123);
#1373=FACE_OUTER_BOUND('',#1983,.T.);
#1374=FACE_OUTER_BOUND('',#1984,.T.);
#1375=FACE_OUTER_BOUND('',#1985,.T.);
#1376=FACE_OUTER_BOUND('',#1986,.T.);
#1377=FACE_OUTER_BOUND('',#1987,.T.);
#1378=FACE_OUTER_BOUND('',#1988,.T.);
#1379=FACE_OUTER_BOUND('',#1989,.T.);
#1380=FACE_OUTER_BOUND('',#1990,.T.);
#1381=FACE_OUTER_BOUND('',#1992,.T.);
#1382=FACE_OUTER_BOUND('',#1994,.T.);
#1383=FACE_OUTER_BOUND('',#1995,.T.);
#1384=FACE_OUTER_BOUND('',#1996,.T.);
#1385=FACE_OUTER_BOUND('',#1997,.T.);
#1386=FACE_OUTER_BOUND('',#2003,.T.);
#1387=FACE_OUTER_BOUND('',#2004,.T.);
#1388=FACE_OUTER_BOUND('',#2010,.T.);
#1389=FACE_OUTER_BOUND('',#2011,.T.);
#1983=EDGE_LOOP('',(#6332,#6333,#6334,#6335));
#1984=EDGE_LOOP('',(#6336,#6337,#6338,#6339));
#1985=EDGE_LOOP('',(#6340,#6341,#6342,#6343));
#1986=EDGE_LOOP('',(#6344,#6345,#6346,#6347));
#1987=EDGE_LOOP('',(#6348,#6349,#6350,#6351));
#1988=EDGE_LOOP('',(#6352,#6353,#6354,#6355));
#1989=EDGE_LOOP('',(#6356,#6357,#6358,#6359));
#1990=EDGE_LOOP('',(#6360,#6361,#6362,#6363));
#1991=EDGE_LOOP('',(#6364));
#1992=EDGE_LOOP('',(#6365,#6366,#6367,#6368));
#1993=EDGE_LOOP('',(#6369));
#1994=EDGE_LOOP('',(#6370,#6371,#6372,#6373));
#1995=EDGE_LOOP('',(#6374,#6375,#6376,#6377));
#1996=EDGE_LOOP('',(#6378,#6379,#6380,#6381,#6382,#6383,#6384,#6385));
#1997=EDGE_LOOP('',(#6386,#6387,#6388,#6389));
#1998=EDGE_LOOP('',(#6390));
#1999=EDGE_LOOP('',(#6391));
#2000=EDGE_LOOP('',(#6392));
#2001=EDGE_LOOP('',(#6393));
#2002=EDGE_LOOP('',(#6394));
#2003=EDGE_LOOP('',(#6395,#6396,#6397,#6398,#6399,#6400,#6401,#6402));
#2004=EDGE_LOOP('',(#6403,#6404,#6405,#6406));
#2005=EDGE_LOOP('',(#6407));
#2006=EDGE_LOOP('',(#6408));
#2007=EDGE_LOOP('',(#6409));
#2008=EDGE_LOOP('',(#6410));
#2009=EDGE_LOOP('',(#6411));
#2010=EDGE_LOOP('',(#6412,#6413,#6414,#6415));
#2011=EDGE_LOOP('',(#6416,#6417,#6418,#6419));
#2012=EDGE_LOOP('',(#6420));
#2013=EDGE_LOOP('',(#6421));
#2606=LINE('',#13225,#3146);
#2607=LINE('',#13231,#3147);
#2608=LINE('',#13237,#3148);
#2609=LINE('',#13243,#3149);
#2610=LINE('',#13249,#3150);
#2611=LINE('',#13255,#3151);
#2612=LINE('',#13261,#3152);
#2613=LINE('',#13266,#3153);
#2614=LINE('',#13268,#3154);
#2615=LINE('',#13270,#3155);
#2616=LINE('',#13271,#3156);
#2617=LINE('',#13275,#3157);
#2618=LINE('',#13277,#3158);
#2619=LINE('',#13279,#3159);
#2620=LINE('',#13280,#3160);
#2621=LINE('',#13283,#3161);
#2622=LINE('',#13285,#3162);
#2623=LINE('',#13286,#3163);
#2624=LINE('',#13289,#3164);
#2625=LINE('',#13291,#3165);
#2626=LINE('',#13292,#3166);
#2627=LINE('',#13295,#3167);
#2628=LINE('',#13297,#3168);
#2629=LINE('',#13298,#3169);
#2630=LINE('',#13299,#3170);
#2631=LINE('',#13302,#3171);
#2632=LINE('',#13303,#3172);
#2633=LINE('',#13306,#3173);
#2634=LINE('',#13307,#3174);
#2635=LINE('',#13308,#3175);
#2636=LINE('',#13310,#3176);
#3146=VECTOR('',#10708,0.165);
#3147=VECTOR('',#10715,0.164999999999999);
#3148=VECTOR('',#10722,0.164999999999999);
#3149=VECTOR('',#10729,0.165);
#3150=VECTOR('',#10736,1.6);
#3151=VECTOR('',#10743,0.225);
#3152=VECTOR('',#10750,0.225);
#3153=VECTOR('',#10755,1.);
#3154=VECTOR('',#10756,1.);
#3155=VECTOR('',#10757,1.);
#3156=VECTOR('',#10758,1.);
#3157=VECTOR('',#10761,1.);
#3158=VECTOR('',#10762,1.);
#3159=VECTOR('',#10763,1.);
#3160=VECTOR('',#10764,1.);
#3161=VECTOR('',#10767,1.);
#3162=VECTOR('',#10768,1.);
#3163=VECTOR('',#10769,1.);
#3164=VECTOR('',#10772,1.);
#3165=VECTOR('',#10773,1.);
#3166=VECTOR('',#10774,1.);
#3167=VECTOR('',#10777,1.);
#3168=VECTOR('',#10778,1.);
#3169=VECTOR('',#10779,1.);
#3170=VECTOR('',#10780,1.);
#3171=VECTOR('',#10783,1.);
#3172=VECTOR('',#10784,1.);
#3173=VECTOR('',#10787,1.);
#3174=VECTOR('',#10788,1.);
#3175=VECTOR('',#10789,1.);
#3176=VECTOR('',#10792,1.);
#3627=CIRCLE('',#9094,0.165);
#3628=CIRCLE('',#9095,0.165);
#3629=CIRCLE('',#9097,0.164999999999999);
#3630=CIRCLE('',#9098,0.164999999999999);
#3631=CIRCLE('',#9100,0.164999999999999);
#3632=CIRCLE('',#9101,0.164999999999999);
#3633=CIRCLE('',#9103,0.165);
#3634=CIRCLE('',#9104,0.165);
#3635=CIRCLE('',#9106,1.6);
#3636=CIRCLE('',#9107,1.6);
#3637=CIRCLE('',#9109,0.225);
#3638=CIRCLE('',#9110,0.225);
#3639=CIRCLE('',#9112,0.225);
#3640=CIRCLE('',#9113,0.225);
#4135=VERTEX_POINT('',#13222);
#4136=VERTEX_POINT('',#13224);
#4137=VERTEX_POINT('',#13228);
#4138=VERTEX_POINT('',#13230);
#4139=VERTEX_POINT('',#13234);
#4140=VERTEX_POINT('',#13236);
#4141=VERTEX_POINT('',#13240);
#4142=VERTEX_POINT('',#13242);
#4143=VERTEX_POINT('',#13246);
#4144=VERTEX_POINT('',#13248);
#4145=VERTEX_POINT('',#13252);
#4146=VERTEX_POINT('',#13254);
#4147=VERTEX_POINT('',#13258);
#4148=VERTEX_POINT('',#13260);
#4149=VERTEX_POINT('',#13264);
#4150=VERTEX_POINT('',#13265);
#4151=VERTEX_POINT('',#13267);
#4152=VERTEX_POINT('',#13269);
#4153=VERTEX_POINT('',#13273);
#4154=VERTEX_POINT('',#13274);
#4155=VERTEX_POINT('',#13276);
#4156=VERTEX_POINT('',#13278);
#4157=VERTEX_POINT('',#13282);
#4158=VERTEX_POINT('',#13284);
#4159=VERTEX_POINT('',#13288);
#4160=VERTEX_POINT('',#13290);
#4161=VERTEX_POINT('',#13294);
#4162=VERTEX_POINT('',#13296);
#4163=VERTEX_POINT('',#13301);
#4164=VERTEX_POINT('',#13305);
#4935=EDGE_CURVE('',#4135,#4135,#3627,.T.);
#4936=EDGE_CURVE('',#4135,#4136,#2606,.T.);
#4937=EDGE_CURVE('',#4136,#4136,#3628,.T.);
#4938=EDGE_CURVE('',#4137,#4137,#3629,.T.);
#4939=EDGE_CURVE('',#4137,#4138,#2607,.T.);
#4940=EDGE_CURVE('',#4138,#4138,#3630,.T.);
#4941=EDGE_CURVE('',#4139,#4139,#3631,.T.);
#4942=EDGE_CURVE('',#4139,#4140,#2608,.T.);
#4943=EDGE_CURVE('',#4140,#4140,#3632,.T.);
#4944=EDGE_CURVE('',#4141,#4141,#3633,.T.);
#4945=EDGE_CURVE('',#4141,#4142,#2609,.T.);
#4946=EDGE_CURVE('',#4142,#4142,#3634,.T.);
#4947=EDGE_CURVE('',#4143,#4143,#3635,.T.);
#4948=EDGE_CURVE('',#4143,#4144,#2610,.T.);
#4949=EDGE_CURVE('',#4144,#4144,#3636,.T.);
#4950=EDGE_CURVE('',#4145,#4145,#3637,.T.);
#4951=EDGE_CURVE('',#4145,#4146,#2611,.T.);
#4952=EDGE_CURVE('',#4146,#4146,#3638,.T.);
#4953=EDGE_CURVE('',#4147,#4147,#3639,.T.);
#4954=EDGE_CURVE('',#4147,#4148,#2612,.T.);
#4955=EDGE_CURVE('',#4148,#4148,#3640,.T.);
#4956=EDGE_CURVE('',#4149,#4150,#2613,.T.);
#4957=EDGE_CURVE('',#4151,#4149,#2614,.T.);
#4958=EDGE_CURVE('',#4151,#4152,#2615,.T.);
#4959=EDGE_CURVE('',#4150,#4152,#2616,.T.);
#4960=EDGE_CURVE('',#4153,#4154,#2617,.T.);
#4961=EDGE_CURVE('',#4155,#4153,#2618,.T.);
#4962=EDGE_CURVE('',#4156,#4155,#2619,.T.);
#4963=EDGE_CURVE('',#4154,#4156,#2620,.T.);
#4964=EDGE_CURVE('',#4156,#4157,#2621,.T.);
#4965=EDGE_CURVE('',#4158,#4155,#2622,.T.);
#4966=EDGE_CURVE('',#4157,#4158,#2623,.T.);
#4967=EDGE_CURVE('',#4159,#4151,#2624,.T.);
#4968=EDGE_CURVE('',#4159,#4160,#2625,.T.);
#4969=EDGE_CURVE('',#4152,#4160,#2626,.T.);
#4970=EDGE_CURVE('',#4149,#4161,#2627,.T.);
#4971=EDGE_CURVE('',#4162,#4161,#2628,.T.);
#4972=EDGE_CURVE('',#4154,#4162,#2629,.T.);
#4973=EDGE_CURVE('',#4157,#4159,#2630,.T.);
#4974=EDGE_CURVE('',#4150,#4163,#2631,.T.);
#4975=EDGE_CURVE('',#4161,#4163,#2632,.T.);
#4976=EDGE_CURVE('',#4153,#4164,#2633,.T.);
#4977=EDGE_CURVE('',#4163,#4164,#2634,.T.);
#4978=EDGE_CURVE('',#4160,#4158,#2635,.T.);
#4979=EDGE_CURVE('',#4164,#4162,#2636,.T.);
#6332=ORIENTED_EDGE('',*,*,#4935,.F.);
#6333=ORIENTED_EDGE('',*,*,#4936,.T.);
#6334=ORIENTED_EDGE('',*,*,#4937,.F.);
#6335=ORIENTED_EDGE('',*,*,#4936,.F.);
#6336=ORIENTED_EDGE('',*,*,#4938,.F.);
#6337=ORIENTED_EDGE('',*,*,#4939,.T.);
#6338=ORIENTED_EDGE('',*,*,#4940,.F.);
#6339=ORIENTED_EDGE('',*,*,#4939,.F.);
#6340=ORIENTED_EDGE('',*,*,#4941,.F.);
#6341=ORIENTED_EDGE('',*,*,#4942,.T.);
#6342=ORIENTED_EDGE('',*,*,#4943,.F.);
#6343=ORIENTED_EDGE('',*,*,#4942,.F.);
#6344=ORIENTED_EDGE('',*,*,#4944,.F.);
#6345=ORIENTED_EDGE('',*,*,#4945,.T.);
#6346=ORIENTED_EDGE('',*,*,#4946,.F.);
#6347=ORIENTED_EDGE('',*,*,#4945,.F.);
#6348=ORIENTED_EDGE('',*,*,#4947,.F.);
#6349=ORIENTED_EDGE('',*,*,#4948,.T.);
#6350=ORIENTED_EDGE('',*,*,#4949,.F.);
#6351=ORIENTED_EDGE('',*,*,#4948,.F.);
#6352=ORIENTED_EDGE('',*,*,#4950,.F.);
#6353=ORIENTED_EDGE('',*,*,#4951,.T.);
#6354=ORIENTED_EDGE('',*,*,#4952,.F.);
#6355=ORIENTED_EDGE('',*,*,#4951,.F.);
#6356=ORIENTED_EDGE('',*,*,#4953,.F.);
#6357=ORIENTED_EDGE('',*,*,#4954,.T.);
#6358=ORIENTED_EDGE('',*,*,#4955,.F.);
#6359=ORIENTED_EDGE('',*,*,#4954,.F.);
#6360=ORIENTED_EDGE('',*,*,#4956,.F.);
#6361=ORIENTED_EDGE('',*,*,#4957,.F.);
#6362=ORIENTED_EDGE('',*,*,#4958,.T.);
#6363=ORIENTED_EDGE('',*,*,#4959,.F.);
#6364=ORIENTED_EDGE('',*,*,#4955,.T.);
#6365=ORIENTED_EDGE('',*,*,#4960,.F.);
#6366=ORIENTED_EDGE('',*,*,#4961,.F.);
#6367=ORIENTED_EDGE('',*,*,#4962,.F.);
#6368=ORIENTED_EDGE('',*,*,#4963,.F.);
#6369=ORIENTED_EDGE('',*,*,#4952,.T.);
#6370=ORIENTED_EDGE('',*,*,#4964,.F.);
#6371=ORIENTED_EDGE('',*,*,#4962,.T.);
#6372=ORIENTED_EDGE('',*,*,#4965,.F.);
#6373=ORIENTED_EDGE('',*,*,#4966,.F.);
#6374=ORIENTED_EDGE('',*,*,#4967,.F.);
#6375=ORIENTED_EDGE('',*,*,#4968,.T.);
#6376=ORIENTED_EDGE('',*,*,#4969,.F.);
#6377=ORIENTED_EDGE('',*,*,#4958,.F.);
#6378=ORIENTED_EDGE('',*,*,#4970,.T.);
#6379=ORIENTED_EDGE('',*,*,#4971,.F.);
#6380=ORIENTED_EDGE('',*,*,#4972,.F.);
#6381=ORIENTED_EDGE('',*,*,#4963,.T.);
#6382=ORIENTED_EDGE('',*,*,#4964,.T.);
#6383=ORIENTED_EDGE('',*,*,#4973,.T.);
#6384=ORIENTED_EDGE('',*,*,#4967,.T.);
#6385=ORIENTED_EDGE('',*,*,#4957,.T.);
#6386=ORIENTED_EDGE('',*,*,#4956,.T.);
#6387=ORIENTED_EDGE('',*,*,#4974,.T.);
#6388=ORIENTED_EDGE('',*,*,#4975,.F.);
#6389=ORIENTED_EDGE('',*,*,#4970,.F.);
#6390=ORIENTED_EDGE('',*,*,#4949,.T.);
#6391=ORIENTED_EDGE('',*,*,#4946,.T.);
#6392=ORIENTED_EDGE('',*,*,#4943,.T.);
#6393=ORIENTED_EDGE('',*,*,#4940,.T.);
#6394=ORIENTED_EDGE('',*,*,#4937,.T.);
#6395=ORIENTED_EDGE('',*,*,#4976,.T.);
#6396=ORIENTED_EDGE('',*,*,#4977,.F.);
#6397=ORIENTED_EDGE('',*,*,#4974,.F.);
#6398=ORIENTED_EDGE('',*,*,#4959,.T.);
#6399=ORIENTED_EDGE('',*,*,#4969,.T.);
#6400=ORIENTED_EDGE('',*,*,#4978,.T.);
#6401=ORIENTED_EDGE('',*,*,#4965,.T.);
#6402=ORIENTED_EDGE('',*,*,#4961,.T.);
#6403=ORIENTED_EDGE('',*,*,#4960,.T.);
#6404=ORIENTED_EDGE('',*,*,#4972,.T.);
#6405=ORIENTED_EDGE('',*,*,#4979,.F.);
#6406=ORIENTED_EDGE('',*,*,#4976,.F.);
#6407=ORIENTED_EDGE('',*,*,#4947,.T.);
#6408=ORIENTED_EDGE('',*,*,#4944,.T.);
#6409=ORIENTED_EDGE('',*,*,#4941,.T.);
#6410=ORIENTED_EDGE('',*,*,#4938,.T.);
#6411=ORIENTED_EDGE('',*,*,#4935,.T.);
#6412=ORIENTED_EDGE('',*,*,#4979,.T.);
#6413=ORIENTED_EDGE('',*,*,#4971,.T.);
#6414=ORIENTED_EDGE('',*,*,#4975,.T.);
#6415=ORIENTED_EDGE('',*,*,#4977,.T.);
#6416=ORIENTED_EDGE('',*,*,#4978,.F.);
#6417=ORIENTED_EDGE('',*,*,#4968,.F.);
#6418=ORIENTED_EDGE('',*,*,#4973,.F.);
#6419=ORIENTED_EDGE('',*,*,#4966,.T.);
#6420=ORIENTED_EDGE('',*,*,#4950,.T.);
#6421=ORIENTED_EDGE('',*,*,#4953,.T.);
#7615=CYLINDRICAL_SURFACE('',#9093,0.165);
#7616=CYLINDRICAL_SURFACE('',#9096,0.164999999999999);
#7617=CYLINDRICAL_SURFACE('',#9099,0.164999999999999);
#7618=CYLINDRICAL_SURFACE('',#9102,0.165);
#7619=CYLINDRICAL_SURFACE('',#9105,1.6);
#7620=CYLINDRICAL_SURFACE('',#9108,0.225);
#7621=CYLINDRICAL_SURFACE('',#9111,0.225);
#7865=ADVANCED_FACE('',(#1373),#7615,.F.);
#7866=ADVANCED_FACE('',(#1374),#7616,.F.);
#7867=ADVANCED_FACE('',(#1375),#7617,.F.);
#7868=ADVANCED_FACE('',(#1376),#7618,.F.);
#7869=ADVANCED_FACE('',(#1377),#7619,.F.);
#7870=ADVANCED_FACE('',(#1378),#7620,.F.);
#7871=ADVANCED_FACE('',(#1379),#7621,.F.);
#7872=ADVANCED_FACE('',(#1380,#859),#1032,.T.);
#7873=ADVANCED_FACE('',(#1381,#860),#1033,.T.);
#7874=ADVANCED_FACE('',(#1382),#1034,.T.);
#7875=ADVANCED_FACE('',(#1383),#1035,.T.);
#7876=ADVANCED_FACE('',(#1384),#1036,.T.);
#7877=ADVANCED_FACE('',(#1385,#861,#862,#863,#864,#865),#1037,.T.);
#7878=ADVANCED_FACE('',(#1386),#1038,.T.);
#7879=ADVANCED_FACE('',(#1387,#866,#867,#868,#869,#870),#1039,.T.);
#7880=ADVANCED_FACE('',(#1388),#1040,.T.);
#7881=ADVANCED_FACE('',(#1389,#871,#872),#1041,.F.);
#8179=CLOSED_SHELL('',(#7865,#7866,#7867,#7868,#7869,#7870,#7871,#7872,
#7873,#7874,#7875,#7876,#7877,#7878,#7879,#7880,#7881));
#9092=AXIS2_PLACEMENT_3D('',#13220,#10702,#10703);
#9093=AXIS2_PLACEMENT_3D('',#13221,#10704,#10705);
#9094=AXIS2_PLACEMENT_3D('',#13223,#10706,#10707);
#9095=AXIS2_PLACEMENT_3D('',#13226,#10709,#10710);
#9096=AXIS2_PLACEMENT_3D('',#13227,#10711,#10712);
#9097=AXIS2_PLACEMENT_3D('',#13229,#10713,#10714);
#9098=AXIS2_PLACEMENT_3D('',#13232,#10716,#10717);
#9099=AXIS2_PLACEMENT_3D('',#13233,#10718,#10719);
#9100=AXIS2_PLACEMENT_3D('',#13235,#10720,#10721);
#9101=AXIS2_PLACEMENT_3D('',#13238,#10723,#10724);
#9102=AXIS2_PLACEMENT_3D('',#13239,#10725,#10726);
#9103=AXIS2_PLACEMENT_3D('',#13241,#10727,#10728);
#9104=AXIS2_PLACEMENT_3D('',#13244,#10730,#10731);
#9105=AXIS2_PLACEMENT_3D('',#13245,#10732,#10733);
#9106=AXIS2_PLACEMENT_3D('',#13247,#10734,#10735);
#9107=AXIS2_PLACEMENT_3D('',#13250,#10737,#10738);
#9108=AXIS2_PLACEMENT_3D('',#13251,#10739,#10740);
#9109=AXIS2_PLACEMENT_3D('',#13253,#10741,#10742);
#9110=AXIS2_PLACEMENT_3D('',#13256,#10744,#10745);
#9111=AXIS2_PLACEMENT_3D('',#13257,#10746,#10747);
#9112=AXIS2_PLACEMENT_3D('',#13259,#10748,#10749);
#9113=AXIS2_PLACEMENT_3D('',#13262,#10751,#10752);
#9114=AXIS2_PLACEMENT_3D('',#13263,#10753,#10754);
#9115=AXIS2_PLACEMENT_3D('',#13272,#10759,#10760);
#9116=AXIS2_PLACEMENT_3D('',#13281,#10765,#10766);
#9117=AXIS2_PLACEMENT_3D('',#13287,#10770,#10771);
#9118=AXIS2_PLACEMENT_3D('',#13293,#10775,#10776);
#9119=AXIS2_PLACEMENT_3D('',#13300,#10781,#10782);
#9120=AXIS2_PLACEMENT_3D('',#13304,#10785,#10786);
#9121=AXIS2_PLACEMENT_3D('',#13309,#10790,#10791);
#9122=AXIS2_PLACEMENT_3D('',#13311,#10793,#10794);
#9123=AXIS2_PLACEMENT_3D('',#13312,#10795,#10796);
#10702=DIRECTION('axis',(0.,0.,1.));
#10703=DIRECTION('refdir',(1.,0.,0.));
#10704=DIRECTION('center_axis',(1.,0.,0.));
#10705=DIRECTION('ref_axis',(0.,0.,-1.));
#10706=DIRECTION('center_axis',(1.,0.,0.));
#10707=DIRECTION('ref_axis',(0.,0.,-1.));
#10708=DIRECTION('',(1.,0.,0.));
#10709=DIRECTION('center_axis',(-1.,0.,0.));
#10710=DIRECTION('ref_axis',(0.,0.,-1.));
#10711=DIRECTION('center_axis',(1.,0.,0.));
#10712=DIRECTION('ref_axis',(0.,0.,-1.));
#10713=DIRECTION('center_axis',(1.,0.,0.));
#10714=DIRECTION('ref_axis',(0.,0.,-1.));
#10715=DIRECTION('',(1.,0.,0.));
#10716=DIRECTION('center_axis',(-1.,0.,0.));
#10717=DIRECTION('ref_axis',(0.,0.,-1.));
#10718=DIRECTION('center_axis',(1.,0.,0.));
#10719=DIRECTION('ref_axis',(0.,0.,-1.));
#10720=DIRECTION('center_axis',(1.,0.,0.));
#10721=DIRECTION('ref_axis',(0.,0.,-1.));
#10722=DIRECTION('',(1.,0.,0.));
#10723=DIRECTION('center_axis',(-1.,0.,0.));
#10724=DIRECTION('ref_axis',(0.,0.,-1.));
#10725=DIRECTION('center_axis',(1.,0.,0.));
#10726=DIRECTION('ref_axis',(0.,0.,-1.));
#10727=DIRECTION('center_axis',(1.,0.,0.));
#10728=DIRECTION('ref_axis',(0.,0.,-1.));
#10729=DIRECTION('',(1.,0.,0.));
#10730=DIRECTION('center_axis',(-1.,0.,0.));
#10731=DIRECTION('ref_axis',(0.,0.,-1.));
#10732=DIRECTION('center_axis',(1.,0.,0.));
#10733=DIRECTION('ref_axis',(0.,0.,-1.));
#10734=DIRECTION('center_axis',(1.,0.,0.));
#10735=DIRECTION('ref_axis',(0.,0.,-1.));
#10736=DIRECTION('',(1.,0.,0.));
#10737=DIRECTION('center_axis',(-1.,0.,0.));
#10738=DIRECTION('ref_axis',(0.,0.,-1.));
#10739=DIRECTION('center_axis',(0.,0.,1.));
#10740=DIRECTION('ref_axis',(1.,0.,0.));
#10741=DIRECTION('center_axis',(0.,0.,1.));
#10742=DIRECTION('ref_axis',(1.,0.,0.));
#10743=DIRECTION('',(0.,0.,1.));
#10744=DIRECTION('center_axis',(0.,0.,-1.));
#10745=DIRECTION('ref_axis',(1.,0.,0.));
#10746=DIRECTION('center_axis',(0.,0.,1.));
#10747=DIRECTION('ref_axis',(1.,0.,0.));
#10748=DIRECTION('center_axis',(0.,0.,1.));
#10749=DIRECTION('ref_axis',(1.,0.,0.));
#10750=DIRECTION('',(0.,0.,1.));
#10751=DIRECTION('center_axis',(0.,0.,-1.));
#10752=DIRECTION('ref_axis',(1.,0.,0.));
#10753=DIRECTION('center_axis',(0.,0.,1.));
#10754=DIRECTION('ref_axis',(1.,0.,0.));
#10755=DIRECTION('',(0.,1.,0.));
#10756=DIRECTION('',(-1.,0.,0.));
#10757=DIRECTION('',(0.,1.,0.));
#10758=DIRECTION('',(1.,0.,0.));
#10759=DIRECTION('center_axis',(0.,0.,1.));
#10760=DIRECTION('ref_axis',(1.,0.,0.));
#10761=DIRECTION('',(0.,-1.,0.));
#10762=DIRECTION('',(1.,0.,0.));
#10763=DIRECTION('',(0.,1.,0.));
#10764=DIRECTION('',(-1.,0.,0.));
#10765=DIRECTION('center_axis',(-1.,0.,0.));
#10766=DIRECTION('ref_axis',(0.,0.,1.));
#10767=DIRECTION('',(0.,0.,-1.));
#10768=DIRECTION('',(0.,0.,1.));
#10769=DIRECTION('',(0.,1.,0.));
#10770=DIRECTION('center_axis',(1.,0.,0.));
#10771=DIRECTION('ref_axis',(0.,0.,-1.));
#10772=DIRECTION('',(0.,0.,1.));
#10773=DIRECTION('',(0.,1.,0.));
#10774=DIRECTION('',(0.,0.,-1.));
#10775=DIRECTION('center_axis',(0.,-1.,0.));
#10776=DIRECTION('ref_axis',(1.,0.,0.));
#10777=DIRECTION('',(0.,0.,1.));
#10778=DIRECTION('',(1.,0.,0.));
#10779=DIRECTION('',(0.,0.,1.));
#10780=DIRECTION('',(1.,0.,0.));
#10781=DIRECTION('center_axis',(1.,0.,0.));
#10782=DIRECTION('ref_axis',(0.,1.,0.));
#10783=DIRECTION('',(0.,0.,1.));
#10784=DIRECTION('',(0.,1.,0.));
#10785=DIRECTION('center_axis',(0.,1.,0.));
#10786=DIRECTION('ref_axis',(-1.,0.,0.));
#10787=DIRECTION('',(0.,0.,1.));
#10788=DIRECTION('',(-1.,0.,0.));
#10789=DIRECTION('',(-1.,0.,0.));
#10790=DIRECTION('center_axis',(-1.,0.,0.));
#10791=DIRECTION('ref_axis',(0.,-1.,0.));
#10792=DIRECTION('',(0.,-1.,0.));
#10793=DIRECTION('center_axis',(0.,0.,1.));
#10794=DIRECTION('ref_axis',(1.,0.,0.));
#10795=DIRECTION('center_axis',(0.,0.,1.));
#10796=DIRECTION('ref_axis',(1.,0.,0.));
#13220=CARTESIAN_POINT('',(0.,0.,0.));
#13221=CARTESIAN_POINT('Origin',(4.6,1.51507575950825,5.51507575950825));
#13222=CARTESIAN_POINT('',(4.7,1.51507575950825,5.68007575950825));
#13223=CARTESIAN_POINT('Origin',(4.7,1.51507575950825,5.51507575950825));
#13224=CARTESIAN_POINT('',(6.3,1.51507575950825,5.68007575950825));
#13225=CARTESIAN_POINT('',(4.6,1.51507575950825,5.68007575950825));
#13226=CARTESIAN_POINT('Origin',(6.3,1.51507575950825,5.51507575950825));
#13227=CARTESIAN_POINT('Origin',(4.6,1.51507575950825,8.48492424049175));
#13228=CARTESIAN_POINT('',(4.7,1.51507575950825,8.64992424049175));
#13229=CARTESIAN_POINT('Origin',(4.7,1.51507575950825,8.48492424049175));
#13230=CARTESIAN_POINT('',(6.3,1.51507575950825,8.64992424049175));
#13231=CARTESIAN_POINT('',(4.6,1.51507575950825,8.64992424049175));
#13232=CARTESIAN_POINT('Origin',(6.3,1.51507575950825,8.48492424049175));
#13233=CARTESIAN_POINT('Origin',(4.6,4.48492424049175,8.48492424049175));
#13234=CARTESIAN_POINT('',(4.7,4.48492424049175,8.64992424049175));
#13235=CARTESIAN_POINT('Origin',(4.7,4.48492424049175,8.48492424049175));
#13236=CARTESIAN_POINT('',(6.3,4.48492424049175,8.64992424049175));
#13237=CARTESIAN_POINT('',(4.6,4.48492424049175,8.64992424049175));
#13238=CARTESIAN_POINT('Origin',(6.3,4.48492424049175,8.48492424049175));
#13239=CARTESIAN_POINT('Origin',(4.6,4.48492424049175,5.51507575950825));
#13240=CARTESIAN_POINT('',(4.7,4.48492424049175,5.68007575950825));
#13241=CARTESIAN_POINT('Origin',(4.7,4.48492424049175,5.51507575950825));
#13242=CARTESIAN_POINT('',(6.3,4.48492424049175,5.68007575950825));
#13243=CARTESIAN_POINT('',(4.6,4.48492424049175,5.68007575950825));
#13244=CARTESIAN_POINT('Origin',(6.3,4.48492424049175,5.51507575950825));
#13245=CARTESIAN_POINT('Origin',(4.6,3.,7.));
#13246=CARTESIAN_POINT('',(4.7,3.,8.6));
#13247=CARTESIAN_POINT('Origin',(4.7,3.,7.));
#13248=CARTESIAN_POINT('',(6.3,3.,8.6));
#13249=CARTESIAN_POINT('',(4.6,3.,8.6));
#13250=CARTESIAN_POINT('Origin',(6.3,3.,7.));
#13251=CARTESIAN_POINT('Origin',(4.1,1.5,1.9));
#13252=CARTESIAN_POINT('',(3.875,1.5,2.));
#13253=CARTESIAN_POINT('Origin',(4.1,1.5,2.));
#13254=CARTESIAN_POINT('',(3.875,1.5,2.8));
#13255=CARTESIAN_POINT('',(3.875,1.5,1.9));
#13256=CARTESIAN_POINT('Origin',(4.1,1.5,2.8));
#13257=CARTESIAN_POINT('Origin',(6.9,4.5,1.9));
#13258=CARTESIAN_POINT('',(6.675,4.5,2.));
#13259=CARTESIAN_POINT('Origin',(6.9,4.5,2.));
#13260=CARTESIAN_POINT('',(6.675,4.5,2.8));
#13261=CARTESIAN_POINT('',(6.675,4.5,1.9));
#13262=CARTESIAN_POINT('Origin',(6.9,4.5,2.8));
#13263=CARTESIAN_POINT('Origin',(3.6,0.6,2.8));
#13264=CARTESIAN_POINT('',(6.3,0.6,2.8));
#13265=CARTESIAN_POINT('',(6.3,5.4,2.8));
#13266=CARTESIAN_POINT('',(6.3,0.6,2.8));
#13267=CARTESIAN_POINT('',(7.4,0.6,2.8));
#13268=CARTESIAN_POINT('',(7.4,0.6,2.8));
#13269=CARTESIAN_POINT('',(7.4,5.4,2.8));
#13270=CARTESIAN_POINT('',(7.4,0.6,2.8));
#13271=CARTESIAN_POINT('',(7.4,5.4,2.8));
#13272=CARTESIAN_POINT('Origin',(3.6,0.6,2.8));
#13273=CARTESIAN_POINT('',(4.7,5.4,2.8));
#13274=CARTESIAN_POINT('',(4.7,0.6,2.8));
#13275=CARTESIAN_POINT('',(4.7,3.,2.8));
#13276=CARTESIAN_POINT('',(3.6,5.4,2.8));
#13277=CARTESIAN_POINT('',(7.4,5.4,2.8));
#13278=CARTESIAN_POINT('',(3.6,0.6,2.8));
#13279=CARTESIAN_POINT('',(3.6,0.6,2.8));
#13280=CARTESIAN_POINT('',(7.4,0.6,2.8));
#13281=CARTESIAN_POINT('Origin',(3.6,0.6,2.));
#13282=CARTESIAN_POINT('',(3.6,0.6,2.));
#13283=CARTESIAN_POINT('',(3.6,0.6,2.8));
#13284=CARTESIAN_POINT('',(3.6,5.4,2.));
#13285=CARTESIAN_POINT('',(3.6,5.4,2.8));
#13286=CARTESIAN_POINT('',(3.6,0.6,2.));
#13287=CARTESIAN_POINT('Origin',(7.4,0.6,2.8));
#13288=CARTESIAN_POINT('',(7.4,0.6,2.));
#13289=CARTESIAN_POINT('',(7.4,0.6,2.));
#13290=CARTESIAN_POINT('',(7.4,5.4,2.));
#13291=CARTESIAN_POINT('',(7.4,0.6,2.));
#13292=CARTESIAN_POINT('',(7.4,5.4,2.));
#13293=CARTESIAN_POINT('Origin',(4.7,0.6,2.));
#13294=CARTESIAN_POINT('',(6.3,0.6,10.));
#13295=CARTESIAN_POINT('',(6.3,0.6,2.));
#13296=CARTESIAN_POINT('',(4.7,0.6,10.));
#13297=CARTESIAN_POINT('',(4.7,0.6,10.));
#13298=CARTESIAN_POINT('',(4.7,0.6,2.));
#13299=CARTESIAN_POINT('',(3.6,0.6,2.));
#13300=CARTESIAN_POINT('Origin',(6.3,0.6,2.));
#13301=CARTESIAN_POINT('',(6.3,5.4,10.));
#13302=CARTESIAN_POINT('',(6.3,5.4,2.));
#13303=CARTESIAN_POINT('',(6.3,0.6,10.));
#13304=CARTESIAN_POINT('Origin',(6.3,5.4,2.));
#13305=CARTESIAN_POINT('',(4.7,5.4,10.));
#13306=CARTESIAN_POINT('',(4.7,5.4,2.));
#13307=CARTESIAN_POINT('',(6.3,5.4,10.));
#13308=CARTESIAN_POINT('',(3.6,5.4,2.));
#13309=CARTESIAN_POINT('Origin',(4.7,5.4,2.));
#13310=CARTESIAN_POINT('',(4.7,5.4,10.));
#13311=CARTESIAN_POINT('Origin',(5.5,3.,10.));
#13312=CARTESIAN_POINT('Origin',(5.5,3.,2.));
#16956=UNCERTAINTY_MEASURE_WITH_UNIT(LENGTH_MEASURE(0.001),#17047,
'DISTANCE_ACCURACY_VALUE',
'Maximum model space distance between geometric entities at asserted c
onnectivities');
#16993=UNCERTAINTY_MEASURE_WITH_UNIT(LENGTH_MEASURE(0.001),#17047,
'DISTANCE_ACCURACY_VALUE',
'Maximum model space distance between geometric entities at asserted c
onnectivities');
#17009=(
GEOMETRIC_REPRESENTATION_CONTEXT(3)
GLOBAL_UNCERTAINTY_ASSIGNED_CONTEXT((#16956))
GLOBAL_UNIT_ASSIGNED_CONTEXT((#17047,#17049,#17050))
REPRESENTATION_CONTEXT('','3D')
);
#17046=(
GEOMETRIC_REPRESENTATION_CONTEXT(3)
GLOBAL_UNCERTAINTY_ASSIGNED_CONTEXT((#16993))
GLOBAL_UNIT_ASSIGNED_CONTEXT((#17047,#17049,#17050))
REPRESENTATION_CONTEXT('','3D')
);
#17047=(
LENGTH_UNIT()
NAMED_UNIT(*)
SI_UNIT(.CENTI.,.METRE.)
);
#17049=(
NAMED_UNIT(*)
PLANE_ANGLE_UNIT()
SI_UNIT($,.RADIAN.)
);
#17050=(
NAMED_UNIT(*)
SI_UNIT($,.STERADIAN.)
SOLID_ANGLE_UNIT()
);
#17066=SHAPE_DEFINITION_REPRESENTATION(#17118,#17273);
#17118=PRODUCT_DEFINITION_SHAPE('',$,#17326);
#17273=SHAPE_REPRESENTATION('',(#9092),#17009);
#17310=PRODUCT_DEFINITION_CONTEXT('part definition',#17468,'design');
#17326=PRODUCT_DEFINITION('Output bearing carrier (1)',
'Output bearing carrier (1)',#17378,#17310);
#17378=PRODUCT_DEFINITION_FORMATION('',$,#17485);
#17468=APPLICATION_CONTEXT(
'Core Data for Automotive Mechanical Design Process');
#17469=PRODUCT_CONTEXT('part definition',#17468,'mechanical');
#17485=PRODUCT('Output bearing carrier (1)','Output bearing carrier (1)',
'Output bearing carrier (1)',(#17469));
#17585=COLOUR_RGB('Grey',0.48,0.52,0.57);
#17586=FILL_AREA_STYLE_COLOUR('',#17585);
#17587=FILL_AREA_STYLE('',(#17586));
#17588=SURFACE_STYLE_FILL_AREA(#17587);
#17589=SURFACE_SIDE_STYLE('',(#17588));
#17590=SURFACE_STYLE_USAGE(.BOTH.,#17589);
#17591=PRESENTATION_STYLE_ASSIGNMENT((#17590));
ENDSEC;
END-ISO-10303-21;
